ISO-10303-21;
HEADER;
/* Generated by software containing ST-Developer
 * from STEP Tools, Inc. (www.steptools.com) 
 */

FILE_DESCRIPTION(
/* description */ ('PAT-122'),
/* implementation_level */ '2;1');

FILE_NAME(
/* name */ 'Bonded foot pad.step',
/* time_stamp */ '2026-10-29T20:20:12-07:00',
/* author */ (''),
/* organization */ (''),
/* preprocessor_version */ 'ST-DEVELOPER v20.2',
/* originating_system */ 'Autodesk Translation Framework v15.17.0.0',
/* authorisation */ '');

FILE_SCHEMA (('AUTOMOTIVE_DESIGN { 1 0 10303 214 3 1 1 }'));
ENDSEC;

DATA;
#10=MECHANICAL_DESIGN_GEOMETRIC_PRESENTATION_REPRESENTATION('',(#492),#10019);
#448=SHAPE_REPRESENTATION_RELATIONSHIP('SRR','None',#10169,#470);
#470=ADVANCED_BREP_SHAPE_REPRESENTATION('',(#514),#9998);
#492=STYLED_ITEM('',(#10341),#514);
#514=MANIFOLD_SOLID_BREP('Body1',#5614);
#533=FACE_BOUND('',#1126,.T.);
#534=FACE_BOUND('',#1128,.T.);
#611=PLANE('',#5899);
#612=PLANE('',#5900);
#829=FACE_OUTER_BOUND('',#1123,.T.);
#830=FACE_OUTER_BOUND('',#1124,.T.);
#831=FACE_OUTER_BOUND('',#1125,.T.);
#832=FACE_OUTER_BOUND('',#1127,.T.);
#1123=EDGE_LOOP('',(#3877,#3878,#3879,#3880));
#1124=EDGE_LOOP('',(#3881,#3882,#3883,#3884));
#1125=EDGE_LOOP('',(#3885));
#1126=EDGE_LOOP('',(#3886));
#1127=EDGE_LOOP('',(#3887));
#1128=EDGE_LOOP('',(#3888));
#1489=LINE('',#8079,#2033);
#1490=LINE('',#8085,#2034);
#2033=VECTOR('',#6454,0.600000000000001);
#2034=VECTOR('',#6461,2.);
#2579=CIRCLE('',#5894,0.600000000000001);
#2580=CIRCLE('',#5895,0.600000000000001);
#2581=CIRCLE('',#5897,2.);
#2582=CIRCLE('',#5898,2.);
#2709=VERTEX_POINT('',#8076);
#2710=VERTEX_POINT('',#8078);
#2711=VERTEX_POINT('',#8082);
#2712=VERTEX_POINT('',#8084);
#3173=EDGE_CURVE('',#2709,#2709,#2579,.T.);
#3174=EDGE_CURVE('',#2709,#2710,#1489,.T.);
#3175=EDGE_CURVE('',#2710,#2710,#2580,.T.);
#3176=EDGE_CURVE('',#2711,#2711,#2581,.T.);
#3177=EDGE_CURVE('',#2711,#2712,#1490,.T.);
#3178=EDGE_CURVE('',#2712,#2712,#2582,.T.);
#3877=ORIENTED_EDGE('',*,*,#3173,.F.);
#3878=ORIENTED_EDGE('',*,*,#3174,.T.);
#3879=ORIENTED_EDGE('',*,*,#3175,.T.);
#3880=ORIENTED_EDGE('',*,*,#3174,.F.);
#3881=ORIENTED_EDGE('',*,*,#3176,.F.);
#3882=ORIENTED_EDGE('',*,*,#3177,.T.);
#3883=ORIENTED_EDGE('',*,*,#3178,.T.);
#3884=ORIENTED_EDGE('',*,*,#3177,.F.);
#3885=ORIENTED_EDGE('',*,*,#3176,.T.);
#3886=ORIENTED_EDGE('',*,*,#3173,.T.);
#3887=ORIENTED_EDGE('',*,*,#3178,.F.);
#3888=ORIENTED_EDGE('',*,*,#3175,.F.);
#5263=CYLINDRICAL_SURFACE('',#5893,0.600000000000001);
#5264=CYLINDRICAL_SURFACE('',#5896,2.);
#5325=ADVANCED_FACE('',(#829),#5263,.F.);
#5326=ADVANCED_FACE('',(#830),#5264,.T.);
#5327=ADVANCED_FACE('',(#831,#533),#611,.T.);
#5328=ADVANCED_FACE('',(#832,#534),#612,.F.);
#5614=CLOSED_SHELL('',(#5325,#5326,#5327,#5328));
#5892=AXIS2_PLACEMENT_3D('',#8074,#6448,#6449);
#5893=AXIS2_PLACEMENT_3D('',#8075,#6450,#6451);
#5894=AXIS2_PLACEMENT_3D('',#8077,#6452,#6453);
#5895=AXIS2_PLACEMENT_3D('',#8080,#6455,#6456);
#5896=AXIS2_PLACEMENT_3D('',#8081,#6457,#6458);
#5897=AXIS2_PLACEMENT_3D('',#8083,#6459,#6460);
#5898=AXIS2_PLACEMENT_3D('',#8086,#6462,#6463);
#5899=AXIS2_PLACEMENT_3D('',#8087,#6464,#6465);
#5900=AXIS2_PLACEMENT_3D('',#8088,#6466,#6467);
#6448=DIRECTION('axis',(0.,0.,1.));
#6449=DIRECTION('refdir',(1.,0.,0.));
#6450=DIRECTION('center_axis',(0.,0.,1.));
#6451=DIRECTION('ref_axis',(1.,0.,0.));
#6452=DIRECTION('center_axis',(0.,0.,-1.));
#6453=DIRECTION('ref_axis',(1.,0.,0.));
#6454=DIRECTION('',(0.,0.,-1.));
#6455=DIRECTION('center_axis',(0.,0.,-1.));
#6456=DIRECTION('ref_axis',(1.,0.,0.));
#6457=DIRECTION('center_axis',(0.,0.,1.));
#6458=DIRECTION('ref_axis',(1.,0.,0.));
#6459=DIRECTION('center_axis',(0.,0.,1.));
#6460=DIRECTION('ref_axis',(1.,0.,0.));
#6461=DIRECTION('',(0.,0.,-1.));
#6462=DIRECTION('center_axis',(0.,0.,1.));
#6463=DIRECTION('ref_axis',(1.,0.,0.));
#6464=DIRECTION('center_axis',(0.,0.,1.));
#6465=DIRECTION('ref_axis',(1.,0.,0.));
#6466=DIRECTION('center_axis',(0.,0.,1.));
#6467=DIRECTION('ref_axis',(1.,0.,0.));
#8074=CARTESIAN_POINT('',(0.,0.,0.));
#8075=CARTESIAN_POINT('Origin',(-19.,-19.,-1.6));
#8076=CARTESIAN_POINT('',(-19.6,-19.,-0.8));
#8077=CARTESIAN_POINT('Origin',(-19.,-19.,-0.8));
#8078=CARTESIAN_POINT('',(-19.6,-19.,-1.6));
#8079=CARTESIAN_POINT('',(-19.6,-19.,-1.6));
#8080=CARTESIAN_POINT('Origin',(-19.,-19.,-1.6));
#8081=CARTESIAN_POINT('Origin',(-19.,-19.,-1.6));
#8082=CARTESIAN_POINT('',(-21.,-19.,-0.8));
#8083=CARTESIAN_POINT('Origin',(-19.,-19.,-0.8));
#8084=CARTESIAN_POINT('',(-21.,-19.,-1.6));
#8085=CARTESIAN_POINT('',(-21.,-19.,-1.6));
#8086=CARTESIAN_POINT('Origin',(-19.,-19.,-1.6));
#8087=CARTESIAN_POINT('Origin',(-19.,-19.,-0.8));
#8088=CARTESIAN_POINT('Origin',(-19.,-19.,-1.6));
#9974=UNCERTAINTY_MEASURE_WITH_UNIT(LENGTH_MEASURE(0.001),#10020,
'DISTANCE_ACCURACY_VALUE',
'Maximum model space distance between geometric entities at asserted c
onnectivities');
#9995=UNCERTAINTY_MEASURE_WITH_UNIT(LENGTH_MEASURE(0.001),#10020,
'DISTANCE_ACCURACY_VALUE',
'Maximum model space distance between geometric entities at asserted c
onnectivities');
#9998=(
GEOMETRIC_REPRESENTATION_CONTEXT(3)
GLOBAL_UNCERTAINTY_ASSIGNED_CONTEXT((#9974))
GLOBAL_UNIT_ASSIGNED_CONTEXT((#10020,#10022,#10023))
REPRESENTATION_CONTEXT('','3D')
);
#10019=(
GEOMETRIC_REPRESENTATION_CONTEXT(3)
GLOBAL_UNCERTAINTY_ASSIGNED_CONTEXT((#9995))
GLOBAL_UNIT_ASSIGNED_CONTEXT((#10020,#10022,#10023))
REPRESENTATION_CONTEXT('','3D')
);
#10020=(
LENGTH_UNIT()
NAMED_UNIT(*)
SI_UNIT(.CENTI.,.METRE.)
);
#10022=(
NAMED_UNIT(*)
PLANE_ANGLE_UNIT()
SI_UNIT($,.RADIAN.)
);
#10023=(
NAMED_UNIT(*)
SI_UNIT($,.STERADIAN.)
SOLID_ANGLE_UNIT()
);
#10026=SHAPE_DEFINITION_REPRESENTATION(#10049,#10169);
#10049=PRODUCT_DEFINITION_SHAPE('',$,#10193);
#10169=SHAPE_REPRESENTATION('',(#5892),#9998);
#10190=PRODUCT_DEFINITION_CONTEXT('part definition',#10261,'design');
#10193=PRODUCT_DEFINITION('Bonded foot pad','Bonded foot pad',
#10216,#10190);
#10216=PRODUCT_DEFINITION_FORMATION('',$,#10265);
#10261=APPLICATION_CONTEXT(
'Core Data for Automotive Mechanical Design Process');
#10262=PRODUCT_CONTEXT('part definition',#10261,'mechanical');
#10265=PRODUCT('Bonded foot pad','Bonded foot pad',
'Bonded foot pad',(#10262));
#10335=COLOUR_RGB('Sky Blue',0.24,0.69,0.87);
#10336=FILL_AREA_STYLE_COLOUR('',#10335);
#10337=FILL_AREA_STYLE('',(#10336));
#10338=SURFACE_STYLE_FILL_AREA(#10337);
#10339=SURFACE_SIDE_STYLE('',(#10338));
#10340=SURFACE_STYLE_USAGE(.BOTH.,#10339);
#10341=PRESENTATION_STYLE_ASSIGNMENT((#10340));
ENDSEC;
END-ISO-10303-21;
